ISO-10303-21;
HEADER;
/* Generated by software containing ST-Developer
 * from STEP Tools, Inc. (www.steptools.com) 
 */

FILE_DESCRIPTION(
/* description */ ('Gear mesh backlash fixture'),
/* implementation_level */ '2;1');

FILE_NAME(
/* name */ 'Socket Set Screw - M4x6.step',
/* time_stamp */ '2026-10-28T03:26:00-07:00',
/* author */ (''),
/* organization */ (''),
/* preprocessor_version */ 'ST-DEVELOPER v20.2',
/* originating_system */ 'Autodesk Translation Framework v15.17.0.0',
/* authorisation */ '');

FILE_SCHEMA (('AUTOMOTIVE_DESIGN { 1 0 10303 214 3 1 1 }'));
ENDSEC;

DATA;
#10=MECHANICAL_DESIGN_GEOMETRIC_PRESENTATION_REPRESENTATION('',(#1049),#57900);
#767=CONICAL_SURFACE('',#14876,0.185,0.785398163397449);
#768=CONICAL_SURFACE('',#14880,0.1625,0.785398163397449);
#942=SHAPE_REPRESENTATION_RELATIONSHIP('SRR','None',#58140,#992);
#992=ADVANCED_BREP_SHAPE_REPRESENTATION('',(#1113),#57873);
#1049=STYLED_ITEM('',(#58472),#1113);
#1113=MANIFOLD_SOLID_BREP('Body1',#13610);
#1280=FACE_BOUND('',#2926,.T.);
#1512=PLANE('',#14867);
#1513=PLANE('',#14868);
#1514=PLANE('',#14869);
#1515=PLANE('',#14870);
#1516=PLANE('',#14871);
#1517=PLANE('',#14872);
#1518=PLANE('',#14873);
#1519=PLANE('',#14874);
#1520=PLANE('',#14882);
#2016=FACE_OUTER_BOUND('',#2918,.T.);
#2017=FACE_OUTER_BOUND('',#2919,.T.);
#2018=FACE_OUTER_BOUND('',#2920,.T.);
#2019=FACE_OUTER_BOUND('',#2921,.T.);
#2020=FACE_OUTER_BOUND('',#2922,.T.);
#2021=FACE_OUTER_BOUND('',#2923,.T.);
#2022=FACE_OUTER_BOUND('',#2924,.T.);
#2023=FACE_OUTER_BOUND('',#2925,.T.);
#2024=FACE_OUTER_BOUND('',#2927,.T.);
#2025=FACE_OUTER_BOUND('',#2928,.T.);
#2026=FACE_OUTER_BOUND('',#2929,.T.);
#2027=FACE_OUTER_BOUND('',#2930,.T.);
#2918=EDGE_LOOP('',(#10365,#10366,#10367,#10368));
#2919=EDGE_LOOP('',(#10369,#10370,#10371,#10372));
#2920=EDGE_LOOP('',(#10373,#10374,#10375,#10376));
#2921=EDGE_LOOP('',(#10377,#10378,#10379,#10380));
#2922=EDGE_LOOP('',(#10381,#10382,#10383,#10384));
#2923=EDGE_LOOP('',(#10385,#10386,#10387,#10388));
#2924=EDGE_LOOP('',(#10389,#10390,#10391,#10392,#10393,#10394));
#2925=EDGE_LOOP('',(#10395));
#2926=EDGE_LOOP('',(#10396,#10397,#10398,#10399,#10400,#10401));
#2927=EDGE_LOOP('',(#10402,#10403,#10404,#10405));
#2928=EDGE_LOOP('',(#10406,#10407,#10408,#10409));
#2929=EDGE_LOOP('',(#10410,#10411,#10412,#10413));
#2930=EDGE_LOOP('',(#10414));
#3819=LINE('',#21296,#4708);
#3820=LINE('',#21298,#4709);
#3821=LINE('',#21300,#4710);
#3822=LINE('',#21301,#4711);
#3823=LINE('',#21304,#4712);
#3824=LINE('',#21306,#4713);
#3825=LINE('',#21307,#4714);
#3826=LINE('',#21310,#4715);
#3827=LINE('',#21312,#4716);
#3828=LINE('',#21313,#4717);
#3829=LINE('',#21316,#4718);
#3830=LINE('',#21318,#4719);
#3831=LINE('',#21319,#4720);
#3832=LINE('',#21322,#4721);
#3833=LINE('',#21324,#4722);
#3834=LINE('',#21325,#4723);
#3835=LINE('',#21327,#4724);
#3836=LINE('',#21328,#4725);
#3837=LINE('',#21336,#4726);
#3838=LINE('',#21340,#4727);
#3839=LINE('',#21344,#4728);
#4708=VECTOR('',#17332,1.);
#4709=VECTOR('',#17333,1.);
#4710=VECTOR('',#17334,1.);
#4711=VECTOR('',#17335,1.);
#4712=VECTOR('',#17338,1.);
#4713=VECTOR('',#17339,1.);
#4714=VECTOR('',#17340,1.);
#4715=VECTOR('',#17343,1.);
#4716=VECTOR('',#17344,1.);
#4717=VECTOR('',#17345,1.);
#4718=VECTOR('',#17348,1.);
#4719=VECTOR('',#17349,1.);
#4720=VECTOR('',#17350,1.);
#4721=VECTOR('',#17353,1.);
#4722=VECTOR('',#17354,1.);
#4723=VECTOR('',#17355,1.);
#4724=VECTOR('',#17358,1.);
#4725=VECTOR('',#17359,1.);
#4726=VECTOR('',#17370,0.185);
#4727=VECTOR('',#17375,0.2);
#4728=VECTOR('',#17380,0.1625);
#5499=CIRCLE('',#14875,0.17);
#5500=CIRCLE('',#14877,0.1954);
#5501=CIRCLE('',#14879,0.1954);
#5502=CIRCLE('',#14881,0.125);
#6279=VERTEX_POINT('',#21294);
#6280=VERTEX_POINT('',#21295);
#6281=VERTEX_POINT('',#21297);
#6282=VERTEX_POINT('',#21299);
#6283=VERTEX_POINT('',#21303);
#6284=VERTEX_POINT('',#21305);
#6285=VERTEX_POINT('',#21309);
#6286=VERTEX_POINT('',#21311);
#6287=VERTEX_POINT('',#21315);
#6288=VERTEX_POINT('',#21317);
#6289=VERTEX_POINT('',#21321);
#6290=VERTEX_POINT('',#21323);
#6291=VERTEX_POINT('',#21331);
#6292=VERTEX_POINT('',#21334);
#6293=VERTEX_POINT('',#21338);
#6294=VERTEX_POINT('',#21342);
#7769=EDGE_CURVE('',#6279,#6280,#3819,.T.);
#7770=EDGE_CURVE('',#6279,#6281,#3820,.T.);
#7771=EDGE_CURVE('',#6281,#6282,#3821,.T.);
#7772=EDGE_CURVE('',#6280,#6282,#3822,.T.);
#7773=EDGE_CURVE('',#6283,#6279,#3823,.T.);
#7774=EDGE_CURVE('',#6283,#6284,#3824,.T.);
#7775=EDGE_CURVE('',#6284,#6281,#3825,.T.);
#7776=EDGE_CURVE('',#6285,#6283,#3826,.T.);
#7777=EDGE_CURVE('',#6285,#6286,#3827,.T.);
#7778=EDGE_CURVE('',#6286,#6284,#3828,.T.);
#7779=EDGE_CURVE('',#6287,#6285,#3829,.T.);
#7780=EDGE_CURVE('',#6287,#6288,#3830,.T.);
#7781=EDGE_CURVE('',#6288,#6286,#3831,.T.);
#7782=EDGE_CURVE('',#6289,#6287,#3832,.T.);
#7783=EDGE_CURVE('',#6289,#6290,#3833,.T.);
#7784=EDGE_CURVE('',#6290,#6288,#3834,.T.);
#7785=EDGE_CURVE('',#6280,#6289,#3835,.T.);
#7786=EDGE_CURVE('',#6282,#6290,#3836,.T.);
#7787=EDGE_CURVE('',#6291,#6291,#5499,.T.);
#7788=EDGE_CURVE('',#6292,#6292,#5500,.T.);
#7789=EDGE_CURVE('',#6292,#6291,#3837,.T.);
#7790=EDGE_CURVE('',#6293,#6293,#5501,.F.);
#7791=EDGE_CURVE('',#6293,#6292,#3838,.T.);
#7792=EDGE_CURVE('',#6294,#6294,#5502,.T.);
#7793=EDGE_CURVE('',#6294,#6293,#3839,.T.);
#10365=ORIENTED_EDGE('',*,*,#7769,.F.);
#10366=ORIENTED_EDGE('',*,*,#7770,.T.);
#10367=ORIENTED_EDGE('',*,*,#7771,.T.);
#10368=ORIENTED_EDGE('',*,*,#7772,.F.);
#10369=ORIENTED_EDGE('',*,*,#7773,.F.);
#10370=ORIENTED_EDGE('',*,*,#7774,.T.);
#10371=ORIENTED_EDGE('',*,*,#7775,.T.);
#10372=ORIENTED_EDGE('',*,*,#7770,.F.);
#10373=ORIENTED_EDGE('',*,*,#7776,.F.);
#10374=ORIENTED_EDGE('',*,*,#7777,.T.);
#10375=ORIENTED_EDGE('',*,*,#7778,.T.);
#10376=ORIENTED_EDGE('',*,*,#7774,.F.);
#10377=ORIENTED_EDGE('',*,*,#7779,.F.);
#10378=ORIENTED_EDGE('',*,*,#7780,.T.);
#10379=ORIENTED_EDGE('',*,*,#7781,.T.);
#10380=ORIENTED_EDGE('',*,*,#7777,.F.);
#10381=ORIENTED_EDGE('',*,*,#7782,.F.);
#10382=ORIENTED_EDGE('',*,*,#7783,.T.);
#10383=ORIENTED_EDGE('',*,*,#7784,.T.);
#10384=ORIENTED_EDGE('',*,*,#7780,.F.);
#10385=ORIENTED_EDGE('',*,*,#7785,.F.);
#10386=ORIENTED_EDGE('',*,*,#7772,.T.);
#10387=ORIENTED_EDGE('',*,*,#7786,.T.);
#10388=ORIENTED_EDGE('',*,*,#7783,.F.);
#10389=ORIENTED_EDGE('',*,*,#7786,.F.);
#10390=ORIENTED_EDGE('',*,*,#7771,.F.);
#10391=ORIENTED_EDGE('',*,*,#7775,.F.);
#10392=ORIENTED_EDGE('',*,*,#7778,.F.);
#10393=ORIENTED_EDGE('',*,*,#7781,.F.);
#10394=ORIENTED_EDGE('',*,*,#7784,.F.);
#10395=ORIENTED_EDGE('',*,*,#7787,.F.);
#10396=ORIENTED_EDGE('',*,*,#7769,.T.);
#10397=ORIENTED_EDGE('',*,*,#7785,.T.);
#10398=ORIENTED_EDGE('',*,*,#7782,.T.);
#10399=ORIENTED_EDGE('',*,*,#7779,.T.);
#10400=ORIENTED_EDGE('',*,*,#7776,.T.);
#10401=ORIENTED_EDGE('',*,*,#7773,.T.);
#10402=ORIENTED_EDGE('',*,*,#7788,.F.);
#10403=ORIENTED_EDGE('',*,*,#7789,.T.);
#10404=ORIENTED_EDGE('',*,*,#7787,.T.);
#10405=ORIENTED_EDGE('',*,*,#7789,.F.);
#10406=ORIENTED_EDGE('',*,*,#7790,.F.);
#10407=ORIENTED_EDGE('',*,*,#7791,.T.);
#10408=ORIENTED_EDGE('',*,*,#7788,.T.);
#10409=ORIENTED_EDGE('',*,*,#7791,.F.);
#10410=ORIENTED_EDGE('',*,*,#7792,.F.);
#10411=ORIENTED_EDGE('',*,*,#7793,.T.);
#10412=ORIENTED_EDGE('',*,*,#7790,.T.);
#10413=ORIENTED_EDGE('',*,*,#7793,.F.);
#10414=ORIENTED_EDGE('',*,*,#7792,.T.);
#12701=CYLINDRICAL_SURFACE('',#14878,0.1954);
#13133=ADVANCED_FACE('',(#2016),#1512,.F.);
#13134=ADVANCED_FACE('',(#2017),#1513,.F.);
#13135=ADVANCED_FACE('',(#2018),#1514,.F.);
#13136=ADVANCED_FACE('',(#2019),#1515,.F.);
#13137=ADVANCED_FACE('',(#2020),#1516,.F.);
#13138=ADVANCED_FACE('',(#2021),#1517,.F.);
#13139=ADVANCED_FACE('',(#2022),#1518,.F.);
#13140=ADVANCED_FACE('',(#2023,#1280),#1519,.T.);
#13141=ADVANCED_FACE('',(#2024),#767,.T.);
#13142=ADVANCED_FACE('',(#2025),#12701,.T.);
#13143=ADVANCED_FACE('',(#2026),#768,.T.);
#13144=ADVANCED_FACE('',(#2027),#1520,.T.);
#13610=CLOSED_SHELL('',(#13133,#13134,#13135,#13136,#13137,#13138,#13139,
#13140,#13141,#13142,#13143,#13144));
#14866=AXIS2_PLACEMENT_3D('',#21292,#17328,#17329);
#14867=AXIS2_PLACEMENT_3D('',#21293,#17330,#17331);
#14868=AXIS2_PLACEMENT_3D('',#21302,#17336,#17337);
#14869=AXIS2_PLACEMENT_3D('',#21308,#17341,#17342);
#14870=AXIS2_PLACEMENT_3D('',#21314,#17346,#17347);
#14871=AXIS2_PLACEMENT_3D('',#21320,#17351,#17352);
#14872=AXIS2_PLACEMENT_3D('',#21326,#17356,#17357);
#14873=AXIS2_PLACEMENT_3D('',#21329,#17360,#17361);
#14874=AXIS2_PLACEMENT_3D('',#21330,#17362,#17363);
#14875=AXIS2_PLACEMENT_3D('',#21332,#17364,#17365);
#14876=AXIS2_PLACEMENT_3D('',#21333,#17366,#17367);
#14877=AXIS2_PLACEMENT_3D('',#21335,#17368,#17369);
#14878=AXIS2_PLACEMENT_3D('',#21337,#17371,#17372);
#14879=AXIS2_PLACEMENT_3D('',#21339,#17373,#17374);
#14880=AXIS2_PLACEMENT_3D('',#21341,#17376,#17377);
#14881=AXIS2_PLACEMENT_3D('',#21343,#17378,#17379);
#14882=AXIS2_PLACEMENT_3D('',#21345,#17381,#17382);
#17328=DIRECTION('axis',(0.,0.,1.));
#17329=DIRECTION('refdir',(1.,0.,0.));
#17330=DIRECTION('center_axis',(0.866025403784439,0.,-0.5));
#17331=DIRECTION('ref_axis',(0.5,0.,0.866025403784439));
#17332=DIRECTION('',(0.5,0.,0.866025403784439));
#17333=DIRECTION('',(0.,-1.,0.));
#17334=DIRECTION('',(0.5,0.,0.866025403784439));
#17335=DIRECTION('',(0.,-1.,0.));
#17336=DIRECTION('center_axis',(1.20185167898973E-16,0.,-1.));
#17337=DIRECTION('ref_axis',(1.,0.,1.20185167898973E-16));
#17338=DIRECTION('',(1.,0.,1.20185167898973E-16));
#17339=DIRECTION('',(0.,-1.,0.));
#17340=DIRECTION('',(1.,0.,1.20185167898973E-16));
#17341=DIRECTION('center_axis',(-0.866025403784439,0.,-0.5));
#17342=DIRECTION('ref_axis',(0.5,0.,-0.866025403784439));
#17343=DIRECTION('',(0.5,0.,-0.866025403784439));
#17344=DIRECTION('',(0.,-1.,0.));
#17345=DIRECTION('',(0.5,0.,-0.866025403784439));
#17346=DIRECTION('center_axis',(-0.866025403784439,0.,0.5));
#17347=DIRECTION('ref_axis',(-0.5,0.,-0.866025403784439));
#17348=DIRECTION('',(-0.5,0.,-0.866025403784439));
#17349=DIRECTION('',(0.,-1.,0.));
#17350=DIRECTION('',(-0.5,0.,-0.866025403784439));
#17351=DIRECTION('center_axis',(-2.40370335797945E-16,0.,1.));
#17352=DIRECTION('ref_axis',(-1.,0.,-2.40370335797945E-16));
#17353=DIRECTION('',(-1.,0.,-2.40370335797945E-16));
#17354=DIRECTION('',(0.,-1.,0.));
#17355=DIRECTION('',(-1.,0.,-2.40370335797945E-16));
#17356=DIRECTION('center_axis',(0.866025403784439,0.,0.5));
#17357=DIRECTION('ref_axis',(-0.5,0.,0.866025403784439));
#17358=DIRECTION('',(-0.5,0.,0.866025403784439));
#17359=DIRECTION('',(-0.5,0.,0.866025403784439));
#17360=DIRECTION('center_axis',(0.,-1.,0.));
#17361=DIRECTION('ref_axis',(0.,0.,-1.));
#17362=DIRECTION('center_axis',(0.,1.,0.));
#17363=DIRECTION('ref_axis',(0.,0.,1.));
#17364=DIRECTION('center_axis',(0.,-1.,0.));
#17365=DIRECTION('ref_axis',(1.,0.,0.));
#17366=DIRECTION('center_axis',(0.,-1.,0.));
#17367=DIRECTION('ref_axis',(1.,0.,0.));
#17368=DIRECTION('center_axis',(0.,-1.,0.));
#17369=DIRECTION('ref_axis',(1.,0.,0.));
#17370=DIRECTION('',(0.707106781186548,0.707106781186547,8.65956056235494E-17));
#17371=DIRECTION('center_axis',(0.,-1.,0.));
#17372=DIRECTION('ref_axis',(1.,0.,0.));
#17373=DIRECTION('center_axis',(0.,1.,0.));
#17374=DIRECTION('ref_axis',(1.,0.,0.));
#17375=DIRECTION('',(0.,1.,0.));
#17376=DIRECTION('center_axis',(0.,1.,0.));
#17377=DIRECTION('ref_axis',(1.,0.,0.));
#17378=DIRECTION('center_axis',(0.,-1.,0.));
#17379=DIRECTION('ref_axis',(1.,0.,0.));
#17380=DIRECTION('',(-0.707106781186548,0.707106781186547,-8.65956056235494E-17));
#17381=DIRECTION('center_axis',(0.,-1.,0.));
#17382=DIRECTION('ref_axis',(0.,0.,-1.));
#21292=CARTESIAN_POINT('',(0.,0.,0.));
#21293=CARTESIAN_POINT('Origin',(0.0577350269189626,0.,-0.1));
#21294=CARTESIAN_POINT('',(0.0577350269189626,0.,-0.1));
#21295=CARTESIAN_POINT('',(0.115470053837925,0.,0.));
#21296=CARTESIAN_POINT('',(0.0934187836487032,0.,-0.0381939203391614));
#21297=CARTESIAN_POINT('',(0.0577350269189626,-0.2,-0.1));
#21298=CARTESIAN_POINT('',(0.0577350269189626,0.,-0.1));
#21299=CARTESIAN_POINT('',(0.115470053837925,-0.2,0.));
#21300=CARTESIAN_POINT('',(0.115470053837925,-0.2,0.));
#21301=CARTESIAN_POINT('',(0.115470053837925,0.,0.));
#21302=CARTESIAN_POINT('Origin',(-0.0577350269189626,0.,-0.1));
#21303=CARTESIAN_POINT('',(-0.0577350269189626,0.,-0.1));
#21304=CARTESIAN_POINT('',(0.0561324865405187,0.,-0.1));
#21305=CARTESIAN_POINT('',(-0.0577350269189626,-0.2,-0.1));
#21306=CARTESIAN_POINT('',(-0.0577350269189626,0.,-0.1));
#21307=CARTESIAN_POINT('',(0.0577350269189626,-0.2,-0.1));
#21308=CARTESIAN_POINT('Origin',(-0.115470053837925,0.,-1.38777878078145E-17));
#21309=CARTESIAN_POINT('',(-0.115470053837925,0.,-1.41410031829988E-17));
#21310=CARTESIAN_POINT('',(-0.0797862971081845,0.,-0.0618060796608387));
#21311=CARTESIAN_POINT('',(-0.115470053837925,-0.2,-1.38777878078145E-17));
#21312=CARTESIAN_POINT('',(-0.115470053837925,0.,-1.41410031829988E-17));
#21313=CARTESIAN_POINT('',(-0.0577350269189626,-0.2,-0.1));
#21314=CARTESIAN_POINT('Origin',(-0.0577350269189626,0.,0.1));
#21315=CARTESIAN_POINT('',(-0.0577350269189626,0.,0.1));
#21316=CARTESIAN_POINT('',(-0.0509187836487033,0.,0.111806079660839));
#21317=CARTESIAN_POINT('',(-0.0577350269189626,-0.2,0.1));
#21318=CARTESIAN_POINT('',(-0.0577350269189626,0.,0.1));
#21319=CARTESIAN_POINT('',(-0.115470053837925,-0.2,-1.41410031829988E-17));
#21320=CARTESIAN_POINT('Origin',(0.0577350269189626,0.,0.1));
#21321=CARTESIAN_POINT('',(0.0577350269189626,0.,0.1));
#21322=CARTESIAN_POINT('',(0.113867513459481,0.,0.1));
#21323=CARTESIAN_POINT('',(0.0577350269189626,-0.2,0.1));
#21324=CARTESIAN_POINT('',(0.0577350269189626,0.,0.1));
#21325=CARTESIAN_POINT('',(-0.0577350269189626,-0.2,0.1));
#21326=CARTESIAN_POINT('Origin',(0.115470053837925,0.,0.));
#21327=CARTESIAN_POINT('',(0.122286297108185,0.,-0.0118060796608386));
#21328=CARTESIAN_POINT('',(0.0577350269189626,-0.2,0.1));
#21329=CARTESIAN_POINT('Origin',(0.,-0.2,0.));
#21330=CARTESIAN_POINT('Origin',(0.17,0.,0.));
#21331=CARTESIAN_POINT('',(-0.17,-8.67361737988404E-18,-2.0818995585505E-17));
#21332=CARTESIAN_POINT('Origin',(0.,0.,0.));
#21333=CARTESIAN_POINT('Origin',(0.,-0.015,0.));
#21334=CARTESIAN_POINT('',(-0.1954,-0.0254,-2.39295984553393E-17));
#21335=CARTESIAN_POINT('Origin',(0.,-0.0254,0.));
#21336=CARTESIAN_POINT('',(-0.185,-0.015,-2.2655965784226E-17));
#21337=CARTESIAN_POINT('Origin',(0.,-0.2775,0.));
#21338=CARTESIAN_POINT('',(-0.1954,-0.5296,2.39295984553393E-17));
#21339=CARTESIAN_POINT('Origin',(0.,-0.5296,0.));
#21340=CARTESIAN_POINT('',(-0.1954,-0.2775,-2.39295984553393E-17));
#21341=CARTESIAN_POINT('Origin',(0.,-0.5625,0.));
#21342=CARTESIAN_POINT('',(-0.125,-0.6,-1.53080849893419E-17));
#21343=CARTESIAN_POINT('Origin',(0.,-0.6,0.));
#21344=CARTESIAN_POINT('',(-0.1625,-0.5625,-1.99005104861445E-17));
#21345=CARTESIAN_POINT('Origin',(0.,-0.6,0.));
#57814=UNCERTAINTY_MEASURE_WITH_UNIT(LENGTH_MEASURE(0.001),#57901,
'DISTANCE_ACCURACY_VALUE',
'Maximum model space distance between geometric entities at asserted c
onnectivities');
#57841=UNCERTAINTY_MEASURE_WITH_UNIT(LENGTH_MEASURE(0.001),#57901,
'DISTANCE_ACCURACY_VALUE',
'Maximum model space distance between geometric entities at asserted c
onnectivities');
#57873=(
GEOMETRIC_REPRESENTATION_CONTEXT(3)
GLOBAL_UNCERTAINTY_ASSIGNED_CONTEXT((#57814))
GLOBAL_UNIT_ASSIGNED_CONTEXT((#57901,#57903,#57904))
REPRESENTATION_CONTEXT('','3D')
);
#57900=(
GEOMETRIC_REPRESENTATION_CONTEXT(3)
GLOBAL_UNCERTAINTY_ASSIGNED_CONTEXT((#57841))
GLOBAL_UNIT_ASSIGNED_CONTEXT((#57901,#57903,#57904))
REPRESENTATION_CONTEXT('','3D')
);
#57901=(
LENGTH_UNIT()
NAMED_UNIT(*)
SI_UNIT(.CENTI.,.METRE.)
);
#57903=(
NAMED_UNIT(*)
PLANE_ANGLE_UNIT()
SI_UNIT($,.RADIAN.)
);
#57904=(
NAMED_UNIT(*)
SI_UNIT($,.STERADIAN.)
SOLID_ANGLE_UNIT()
);
#57936=SHAPE_DEFINITION_REPRESENTATION(#58002,#58140);
#58002=PRODUCT_DEFINITION_SHAPE('',$,#58199);
#58140=SHAPE_REPRESENTATION('',(#14866),#57873);
#58167=PRODUCT_DEFINITION_CONTEXT('part definition',#58343,'design');
#58199=PRODUCT_DEFINITION('Socket Set Screw - M4x6',
'Socket Set Screw - M4x6',#58257,#58167);
#58257=PRODUCT_DEFINITION_FORMATION('',$,#58376);
#58343=APPLICATION_CONTEXT(
'Core Data for Automotive Mechanical Design Process');
#58344=PRODUCT_CONTEXT('part definition',#58343,'mechanical');
#58376=PRODUCT('Socket Set Screw - M4x6','Socket Set Screw - M4x6',
'Socket Set Screw - M4x6',(#58344));
#58466=COLOUR_RGB('Black',0.12,0.14,0.17);
#58467=FILL_AREA_STYLE_COLOUR('',#58466);
#58468=FILL_AREA_STYLE('',(#58467));
#58469=SURFACE_STYLE_FILL_AREA(#58468);
#58470=SURFACE_SIDE_STYLE('',(#58469));
#58471=SURFACE_STYLE_USAGE(.BOTH.,#58470);
#58472=PRESENTATION_STYLE_ASSIGNMENT((#58471));
ENDSEC;
END-ISO-10303-21;
